ISO-10303-21;
HEADER;
/* Generated by software containing ST-Developer
 * from STEP Tools, Inc. (www.steptools.com) 
 */

FILE_DESCRIPTION(
/* description */ ('Manual rail carriage with stops'),
/* implementation_level */ '2;1');

FILE_NAME(
/* name */ 'Cap Screw - M4x16.step',
/* time_stamp */ '2026-10-27T18:54:27-07:00',
/* author */ (''),
/* organization */ (''),
/* preprocessor_version */ 'ST-DEVELOPER v20.2',
/* originating_system */ 'Autodesk Translation Framework v15.17.0.0',
/* authorisation */ '');

FILE_SCHEMA (('AUTOMOTIVE_DESIGN { 1 0 10303 214 3 1 1 }'));
ENDSEC;

DATA;
#10=MECHANICAL_DESIGN_GEOMETRIC_PRESENTATION_REPRESENTATION('',(#278),#8499);
#214=CONICAL_SURFACE('',#5354,0.325,0.785398163397448);
#215=CONICAL_SURFACE('',#5358,0.335,0.785398163397448);
#216=CONICAL_SURFACE('',#5362,0.21,0.463647609000806);
#217=CONICAL_SURFACE('',#5366,0.18,0.785398163397448);
#228=ORIENTED_CLOSED_SHELL('',*,#4948,.F.);
#232=BREP_WITH_VOIDS('Body1',#4947,(#228));
#242=SHAPE_REPRESENTATION_RELATIONSHIP('SRR','None',#8605,#260);
#260=ADVANCED_BREP_SHAPE_REPRESENTATION('',(#232),#8484);
#278=STYLED_ITEM('',(#8795),#232);
#349=FACE_BOUND('',#1014,.T.);
#474=PLANE('',#5352);
#475=PLANE('',#5360);
#476=PLANE('',#5368);
#477=PLANE('',#5369);
#478=PLANE('',#5370);
#479=PLANE('',#5371);
#480=PLANE('',#5372);
#481=PLANE('',#5373);
#482=PLANE('',#5374);
#483=PLANE('',#5375);
#484=PLANE('',#5376);
#700=FACE_OUTER_BOUND('',#1009,.T.);
#701=FACE_OUTER_BOUND('',#1010,.T.);
#702=FACE_OUTER_BOUND('',#1011,.T.);
#703=FACE_OUTER_BOUND('',#1012,.T.);
#704=FACE_OUTER_BOUND('',#1013,.T.);
#705=FACE_OUTER_BOUND('',#1015,.T.);
#706=FACE_OUTER_BOUND('',#1016,.T.);
#707=FACE_OUTER_BOUND('',#1017,.T.);
#708=FACE_OUTER_BOUND('',#1018,.T.);
#709=FACE_OUTER_BOUND('',#1019,.T.);
#710=FACE_OUTER_BOUND('',#1020,.T.);
#711=FACE_OUTER_BOUND('',#1021,.T.);
#712=FACE_OUTER_BOUND('',#1022,.T.);
#713=FACE_OUTER_BOUND('',#1023,.T.);
#714=FACE_OUTER_BOUND('',#1024,.T.);
#715=FACE_OUTER_BOUND('',#1025,.T.);
#716=FACE_OUTER_BOUND('',#1026,.T.);
#1009=EDGE_LOOP('',(#3996));
#1010=EDGE_LOOP('',(#3997,#3998,#3999,#4000));
#1011=EDGE_LOOP('',(#4001,#4002,#4003,#4004));
#1012=EDGE_LOOP('',(#4005,#4006,#4007,#4008));
#1013=EDGE_LOOP('',(#4009));
#1014=EDGE_LOOP('',(#4010));
#1015=EDGE_LOOP('',(#4011,#4012,#4013,#4014));
#1016=EDGE_LOOP('',(#4015,#4016,#4017,#4018));
#1017=EDGE_LOOP('',(#4019,#4020,#4021,#4022));
#1018=EDGE_LOOP('',(#4023));
#1019=EDGE_LOOP('',(#4024,#4025,#4026,#4027));
#1020=EDGE_LOOP('',(#4028,#4029,#4030,#4031));
#1021=EDGE_LOOP('',(#4032,#4033,#4034,#4035));
#1022=EDGE_LOOP('',(#4036,#4037,#4038,#4039));
#1023=EDGE_LOOP('',(#4040,#4041,#4042,#4043));
#1024=EDGE_LOOP('',(#4044,#4045,#4046,#4047));
#1025=EDGE_LOOP('',(#4048,#4049,#4050,#4051,#4052,#4053));
#1026=EDGE_LOOP('',(#4054,#4055,#4056,#4057,#4058,#4059));
#1441=LINE('',#7735,#1941);
#1442=LINE('',#7739,#1942);
#1443=LINE('',#7743,#1943);
#1444=LINE('',#7750,#1944);
#1445=LINE('',#7754,#1945);
#1446=LINE('',#7758,#1946);
#1447=LINE('',#7763,#1947);
#1448=LINE('',#7765,#1948);
#1449=LINE('',#7767,#1949);
#1450=LINE('',#7768,#1950);
#1451=LINE('',#7771,#1951);
#1452=LINE('',#7773,#1952);
#1453=LINE('',#7774,#1953);
#1454=LINE('',#7777,#1954);
#1455=LINE('',#7779,#1955);
#1456=LINE('',#7780,#1956);
#1457=LINE('',#7783,#1957);
#1458=LINE('',#7785,#1958);
#1459=LINE('',#7786,#1959);
#1460=LINE('',#7789,#1960);
#1461=LINE('',#7791,#1961);
#1462=LINE('',#7792,#1962);
#1463=LINE('',#7794,#1963);
#1464=LINE('',#7795,#1964);
#1941=VECTOR('',#6278,0.325);
#1942=VECTOR('',#6283,0.35);
#1943=VECTOR('',#6288,0.335);
#1944=VECTOR('',#6297,0.21);
#1945=VECTOR('',#6302,0.2);
#1946=VECTOR('',#6307,0.18);
#1947=VECTOR('',#6312,1.);
#1948=VECTOR('',#6313,1.);
#1949=VECTOR('',#6314,1.);
#1950=VECTOR('',#6315,1.);
#1951=VECTOR('',#6318,1.);
#1952=VECTOR('',#6319,1.);
#1953=VECTOR('',#6320,1.);
#1954=VECTOR('',#6323,1.);
#1955=VECTOR('',#6324,1.);
#1956=VECTOR('',#6325,1.);
#1957=VECTOR('',#6328,1.);
#1958=VECTOR('',#6329,1.);
#1959=VECTOR('',#6330,1.);
#1960=VECTOR('',#6333,1.);
#1961=VECTOR('',#6334,1.);
#1962=VECTOR('',#6335,1.);
#1963=VECTOR('',#6338,1.);
#1964=VECTOR('',#6339,1.);
#2239=CIRCLE('',#5353,0.3);
#2240=CIRCLE('',#5355,0.35);
#2241=CIRCLE('',#5357,0.35);
#2242=CIRCLE('',#5359,0.32);
#2243=CIRCLE('',#5361,0.22);
#2244=CIRCLE('',#5363,0.1954);
#2245=CIRCLE('',#5365,0.1954);
#2246=CIRCLE('',#5367,0.16);
#2523=VERTEX_POINT('',#7730);
#2524=VERTEX_POINT('',#7733);
#2525=VERTEX_POINT('',#7737);
#2526=VERTEX_POINT('',#7741);
#2527=VERTEX_POINT('',#7745);
#2528=VERTEX_POINT('',#7748);
#2529=VERTEX_POINT('',#7752);
#2530=VERTEX_POINT('',#7756);
#2531=VERTEX_POINT('',#7761);
#2532=VERTEX_POINT('',#7762);
#2533=VERTEX_POINT('',#7764);
#2534=VERTEX_POINT('',#7766);
#2535=VERTEX_POINT('',#7770);
#2536=VERTEX_POINT('',#7772);
#2537=VERTEX_POINT('',#7776);
#2538=VERTEX_POINT('',#7778);
#2539=VERTEX_POINT('',#7782);
#2540=VERTEX_POINT('',#7784);
#2541=VERTEX_POINT('',#7788);
#2542=VERTEX_POINT('',#7790);
#3046=EDGE_CURVE('',#2523,#2523,#2239,.T.);
#3047=EDGE_CURVE('',#2524,#2524,#2240,.T.);
#3048=EDGE_CURVE('',#2524,#2523,#1441,.T.);
#3049=EDGE_CURVE('',#2525,#2525,#2241,.T.);
#3050=EDGE_CURVE('',#2525,#2524,#1442,.T.);
#3051=EDGE_CURVE('',#2526,#2526,#2242,.T.);
#3052=EDGE_CURVE('',#2526,#2525,#1443,.T.);
#3053=EDGE_CURVE('',#2527,#2527,#2243,.T.);
#3054=EDGE_CURVE('',#2528,#2528,#2244,.F.);
#3055=EDGE_CURVE('',#2528,#2527,#1444,.T.);
#3056=EDGE_CURVE('',#2529,#2529,#2245,.F.);
#3057=EDGE_CURVE('',#2529,#2528,#1445,.T.);
#3058=EDGE_CURVE('',#2530,#2530,#2246,.T.);
#3059=EDGE_CURVE('',#2530,#2529,#1446,.T.);
#3060=EDGE_CURVE('',#2531,#2532,#1447,.T.);
#3061=EDGE_CURVE('',#2532,#2533,#1448,.T.);
#3062=EDGE_CURVE('',#2533,#2534,#1449,.T.);
#3063=EDGE_CURVE('',#2531,#2534,#1450,.T.);
#3064=EDGE_CURVE('',#2532,#2535,#1451,.T.);
#3065=EDGE_CURVE('',#2535,#2536,#1452,.T.);
#3066=EDGE_CURVE('',#2536,#2533,#1453,.T.);
#3067=EDGE_CURVE('',#2535,#2537,#1454,.T.);
#3068=EDGE_CURVE('',#2537,#2538,#1455,.T.);
#3069=EDGE_CURVE('',#2538,#2536,#1456,.T.);
#3070=EDGE_CURVE('',#2537,#2539,#1457,.T.);
#3071=EDGE_CURVE('',#2539,#2540,#1458,.T.);
#3072=EDGE_CURVE('',#2540,#2538,#1459,.T.);
#3073=EDGE_CURVE('',#2539,#2541,#1460,.T.);
#3074=EDGE_CURVE('',#2541,#2542,#1461,.T.);
#3075=EDGE_CURVE('',#2542,#2540,#1462,.T.);
#3076=EDGE_CURVE('',#2541,#2531,#1463,.T.);
#3077=EDGE_CURVE('',#2534,#2542,#1464,.T.);
#3996=ORIENTED_EDGE('',*,*,#3046,.F.);
#3997=ORIENTED_EDGE('',*,*,#3047,.F.);
#3998=ORIENTED_EDGE('',*,*,#3048,.T.);
#3999=ORIENTED_EDGE('',*,*,#3046,.T.);
#4000=ORIENTED_EDGE('',*,*,#3048,.F.);
#4001=ORIENTED_EDGE('',*,*,#3049,.F.);
#4002=ORIENTED_EDGE('',*,*,#3050,.T.);
#4003=ORIENTED_EDGE('',*,*,#3047,.T.);
#4004=ORIENTED_EDGE('',*,*,#3050,.F.);
#4005=ORIENTED_EDGE('',*,*,#3051,.F.);
#4006=ORIENTED_EDGE('',*,*,#3052,.T.);
#4007=ORIENTED_EDGE('',*,*,#3049,.T.);
#4008=ORIENTED_EDGE('',*,*,#3052,.F.);
#4009=ORIENTED_EDGE('',*,*,#3051,.T.);
#4010=ORIENTED_EDGE('',*,*,#3053,.F.);
#4011=ORIENTED_EDGE('',*,*,#3054,.F.);
#4012=ORIENTED_EDGE('',*,*,#3055,.T.);
#4013=ORIENTED_EDGE('',*,*,#3053,.T.);
#4014=ORIENTED_EDGE('',*,*,#3055,.F.);
#4015=ORIENTED_EDGE('',*,*,#3056,.F.);
#4016=ORIENTED_EDGE('',*,*,#3057,.T.);
#4017=ORIENTED_EDGE('',*,*,#3054,.T.);
#4018=ORIENTED_EDGE('',*,*,#3057,.F.);
#4019=ORIENTED_EDGE('',*,*,#3058,.F.);
#4020=ORIENTED_EDGE('',*,*,#3059,.T.);
#4021=ORIENTED_EDGE('',*,*,#3056,.T.);
#4022=ORIENTED_EDGE('',*,*,#3059,.F.);
#4023=ORIENTED_EDGE('',*,*,#3058,.T.);
#4024=ORIENTED_EDGE('',*,*,#3060,.T.);
#4025=ORIENTED_EDGE('',*,*,#3061,.T.);
#4026=ORIENTED_EDGE('',*,*,#3062,.T.);
#4027=ORIENTED_EDGE('',*,*,#3063,.F.);
#4028=ORIENTED_EDGE('',*,*,#3064,.T.);
#4029=ORIENTED_EDGE('',*,*,#3065,.T.);
#4030=ORIENTED_EDGE('',*,*,#3066,.T.);
#4031=ORIENTED_EDGE('',*,*,#3061,.F.);
#4032=ORIENTED_EDGE('',*,*,#3067,.T.);
#4033=ORIENTED_EDGE('',*,*,#3068,.T.);
#4034=ORIENTED_EDGE('',*,*,#3069,.T.);
#4035=ORIENTED_EDGE('',*,*,#3065,.F.);
#4036=ORIENTED_EDGE('',*,*,#3070,.T.);
#4037=ORIENTED_EDGE('',*,*,#3071,.T.);
#4038=ORIENTED_EDGE('',*,*,#3072,.T.);
#4039=ORIENTED_EDGE('',*,*,#3068,.F.);
#4040=ORIENTED_EDGE('',*,*,#3073,.T.);
#4041=ORIENTED_EDGE('',*,*,#3074,.T.);
#4042=ORIENTED_EDGE('',*,*,#3075,.T.);
#4043=ORIENTED_EDGE('',*,*,#3071,.F.);
#4044=ORIENTED_EDGE('',*,*,#3076,.T.);
#4045=ORIENTED_EDGE('',*,*,#3063,.T.);
#4046=ORIENTED_EDGE('',*,*,#3077,.T.);
#4047=ORIENTED_EDGE('',*,*,#3074,.F.);
#4048=ORIENTED_EDGE('',*,*,#3076,.F.);
#4049=ORIENTED_EDGE('',*,*,#3073,.F.);
#4050=ORIENTED_EDGE('',*,*,#3070,.F.);
#4051=ORIENTED_EDGE('',*,*,#3067,.F.);
#4052=ORIENTED_EDGE('',*,*,#3064,.F.);
#4053=ORIENTED_EDGE('',*,*,#3060,.F.);
#4054=ORIENTED_EDGE('',*,*,#3077,.F.);
#4055=ORIENTED_EDGE('',*,*,#3062,.F.);
#4056=ORIENTED_EDGE('',*,*,#3066,.F.);
#4057=ORIENTED_EDGE('',*,*,#3069,.F.);
#4058=ORIENTED_EDGE('',*,*,#3072,.F.);
#4059=ORIENTED_EDGE('',*,*,#3075,.F.);
#4650=CYLINDRICAL_SURFACE('',#5356,0.35);
#4651=CYLINDRICAL_SURFACE('',#5364,0.1954);
#4799=ADVANCED_FACE('',(#700),#474,.T.);
#4800=ADVANCED_FACE('',(#701),#214,.T.);
#4801=ADVANCED_FACE('',(#702),#4650,.T.);
#4802=ADVANCED_FACE('',(#703),#215,.T.);
#4803=ADVANCED_FACE('',(#704,#349),#475,.T.);
#4804=ADVANCED_FACE('',(#705),#216,.T.);
#4805=ADVANCED_FACE('',(#706),#4651,.T.);
#4806=ADVANCED_FACE('',(#707),#217,.T.);
#4807=ADVANCED_FACE('',(#708),#476,.T.);
#4808=ADVANCED_FACE('',(#709),#477,.F.);
#4809=ADVANCED_FACE('',(#710),#478,.F.);
#4810=ADVANCED_FACE('',(#711),#479,.F.);
#4811=ADVANCED_FACE('',(#712),#480,.F.);
#4812=ADVANCED_FACE('',(#713),#481,.F.);
#4813=ADVANCED_FACE('',(#714),#482,.F.);
#4814=ADVANCED_FACE('',(#715),#483,.F.);
#4815=ADVANCED_FACE('',(#716),#484,.F.);
#4947=CLOSED_SHELL('',(#4799,#4800,#4801,#4802,#4803,#4804,#4805,#4806,
#4807));
#4948=CLOSED_SHELL('',(#4808,#4809,#4810,#4811,#4812,#4813,#4814,#4815));
#5351=AXIS2_PLACEMENT_3D('',#7728,#6268,#6269);
#5352=AXIS2_PLACEMENT_3D('',#7729,#6270,#6271);
#5353=AXIS2_PLACEMENT_3D('',#7731,#6272,#6273);
#5354=AXIS2_PLACEMENT_3D('',#7732,#6274,#6275);
#5355=AXIS2_PLACEMENT_3D('',#7734,#6276,#6277);
#5356=AXIS2_PLACEMENT_3D('',#7736,#6279,#6280);
#5357=AXIS2_PLACEMENT_3D('',#7738,#6281,#6282);
#5358=AXIS2_PLACEMENT_3D('',#7740,#6284,#6285);
#5359=AXIS2_PLACEMENT_3D('',#7742,#6286,#6287);
#5360=AXIS2_PLACEMENT_3D('',#7744,#6289,#6290);
#5361=AXIS2_PLACEMENT_3D('',#7746,#6291,#6292);
#5362=AXIS2_PLACEMENT_3D('',#7747,#6293,#6294);
#5363=AXIS2_PLACEMENT_3D('',#7749,#6295,#6296);
#5364=AXIS2_PLACEMENT_3D('',#7751,#6298,#6299);
#5365=AXIS2_PLACEMENT_3D('',#7753,#6300,#6301);
#5366=AXIS2_PLACEMENT_3D('',#7755,#6303,#6304);
#5367=AXIS2_PLACEMENT_3D('',#7757,#6305,#6306);
#5368=AXIS2_PLACEMENT_3D('',#7759,#6308,#6309);
#5369=AXIS2_PLACEMENT_3D('',#7760,#6310,#6311);
#5370=AXIS2_PLACEMENT_3D('',#7769,#6316,#6317);
#5371=AXIS2_PLACEMENT_3D('',#7775,#6321,#6322);
#5372=AXIS2_PLACEMENT_3D('',#7781,#6326,#6327);
#5373=AXIS2_PLACEMENT_3D('',#7787,#6331,#6332);
#5374=AXIS2_PLACEMENT_3D('',#7793,#6336,#6337);
#5375=AXIS2_PLACEMENT_3D('',#7796,#6340,#6341);
#5376=AXIS2_PLACEMENT_3D('',#7797,#6342,#6343);
#6268=DIRECTION('axis',(0.,0.,1.));
#6269=DIRECTION('refdir',(1.,0.,0.));
#6270=DIRECTION('center_axis',(0.,1.,0.));
#6271=DIRECTION('ref_axis',(0.,0.,1.));
#6272=DIRECTION('center_axis',(0.,-1.,0.));
#6273=DIRECTION('ref_axis',(1.,0.,0.));
#6274=DIRECTION('center_axis',(0.,-1.,0.));
#6275=DIRECTION('ref_axis',(1.,0.,0.));
#6276=DIRECTION('center_axis',(0.,-1.,0.));
#6277=DIRECTION('ref_axis',(1.,0.,0.));
#6278=DIRECTION('',(0.707106781186547,0.707106781186548,8.65956056235493E-17));
#6279=DIRECTION('center_axis',(0.,-1.,0.));
#6280=DIRECTION('ref_axis',(1.,0.,0.));
#6281=DIRECTION('center_axis',(0.,-1.,0.));
#6282=DIRECTION('ref_axis',(1.,0.,0.));
#6283=DIRECTION('',(0.,1.,0.));
#6284=DIRECTION('center_axis',(0.,1.,0.));
#6285=DIRECTION('ref_axis',(1.,0.,0.));
#6286=DIRECTION('center_axis',(0.,-1.,0.));
#6287=DIRECTION('ref_axis',(1.,0.,0.));
#6288=DIRECTION('',(-0.707106781186547,0.707106781186548,-8.65956056235493E-17));
#6289=DIRECTION('center_axis',(0.,-1.,0.));
#6290=DIRECTION('ref_axis',(0.,0.,-1.));
#6291=DIRECTION('center_axis',(0.,-1.,0.));
#6292=DIRECTION('ref_axis',(1.,0.,0.));
#6293=DIRECTION('center_axis',(0.,1.,0.));
#6294=DIRECTION('ref_axis',(1.,0.,0.));
#6295=DIRECTION('center_axis',(0.,1.,0.));
#6296=DIRECTION('ref_axis',(1.,0.,0.));
#6297=DIRECTION('',(-0.447213595499958,0.894427190999916,-5.47678698264203E-17));
#6298=DIRECTION('center_axis',(0.,-1.,0.));
#6299=DIRECTION('ref_axis',(1.,0.,0.));
#6300=DIRECTION('center_axis',(0.,1.,0.));
#6301=DIRECTION('ref_axis',(1.,0.,0.));
#6302=DIRECTION('',(0.,1.,0.));
#6303=DIRECTION('center_axis',(0.,1.,0.));
#6304=DIRECTION('ref_axis',(1.,0.,0.));
#6305=DIRECTION('center_axis',(0.,-1.,0.));
#6306=DIRECTION('ref_axis',(1.,0.,0.));
#6307=DIRECTION('',(-0.707106781186547,0.707106781186548,-8.65956056235493E-17));
#6308=DIRECTION('center_axis',(0.,-1.,0.));
#6309=DIRECTION('ref_axis',(0.,0.,-1.));
#6310=DIRECTION('center_axis',(0.866025403784439,0.,-0.5));
#6311=DIRECTION('ref_axis',(0.5,0.,0.866025403784439));
#6312=DIRECTION('',(-0.5,0.,-0.866025403784439));
#6313=DIRECTION('',(0.,-1.,0.));
#6314=DIRECTION('',(0.5,0.,0.866025403784439));
#6315=DIRECTION('',(0.,-1.,0.));
#6316=DIRECTION('center_axis',(1.60246890531964E-16,0.,-1.));
#6317=DIRECTION('ref_axis',(1.,0.,1.60246890531964E-16));
#6318=DIRECTION('',(-1.,0.,-1.60246890531964E-16));
#6319=DIRECTION('',(0.,-1.,0.));
#6320=DIRECTION('',(1.,0.,1.60246890531964E-16));
#6321=DIRECTION('center_axis',(-0.866025403784439,0.,-0.5));
#6322=DIRECTION('ref_axis',(0.5,0.,-0.866025403784439));
#6323=DIRECTION('',(-0.5,0.,0.866025403784439));
#6324=DIRECTION('',(0.,-1.,0.));
#6325=DIRECTION('',(0.5,0.,-0.866025403784439));
#6326=DIRECTION('center_axis',(-0.866025403784439,0.,0.5));
#6327=DIRECTION('ref_axis',(-0.5,0.,-0.866025403784439));
#6328=DIRECTION('',(0.5,0.,0.866025403784439));
#6329=DIRECTION('',(0.,-1.,0.));
#6330=DIRECTION('',(-0.5,0.,-0.866025403784439));
#6331=DIRECTION('center_axis',(-1.60246890531964E-16,0.,1.));
#6332=DIRECTION('ref_axis',(-1.,0.,-1.60246890531964E-16));
#6333=DIRECTION('',(1.,0.,1.60246890531964E-16));
#6334=DIRECTION('',(0.,-1.,0.));
#6335=DIRECTION('',(-1.,0.,-1.60246890531964E-16));
#6336=DIRECTION('center_axis',(0.866025403784439,0.,0.5));
#6337=DIRECTION('ref_axis',(-0.5,0.,0.866025403784439));
#6338=DIRECTION('',(0.5,0.,-0.866025403784439));
#6339=DIRECTION('',(-0.5,0.,0.866025403784439));
#6340=DIRECTION('center_axis',(0.,1.,0.));
#6341=DIRECTION('ref_axis',(1.,0.,0.));
#6342=DIRECTION('center_axis',(0.,-1.,0.));
#6343=DIRECTION('ref_axis',(0.,0.,-1.));
#7728=CARTESIAN_POINT('',(0.,0.,0.));
#7729=CARTESIAN_POINT('Origin',(0.3,0.4,0.));
#7730=CARTESIAN_POINT('',(-0.3,0.4,-3.67394039744206E-17));
#7731=CARTESIAN_POINT('Origin',(0.,0.4,0.));
#7732=CARTESIAN_POINT('Origin',(0.,0.375,0.));
#7733=CARTESIAN_POINT('',(-0.35,0.35,-4.28626379701573E-17));
#7734=CARTESIAN_POINT('Origin',(0.,0.35,0.));
#7735=CARTESIAN_POINT('',(-0.325,0.375,-3.9801020972289E-17));
#7736=CARTESIAN_POINT('Origin',(0.,0.19,0.));
#7737=CARTESIAN_POINT('',(-0.35,0.03,-4.28626379701574E-17));
#7738=CARTESIAN_POINT('Origin',(0.,0.03,0.));
#7739=CARTESIAN_POINT('',(-0.35,0.19,-4.28626379701574E-17));
#7740=CARTESIAN_POINT('Origin',(0.,0.0149999999999999,0.));
#7741=CARTESIAN_POINT('',(-0.32,-3.29597460435593E-17,-3.91886975727153E-17));
#7742=CARTESIAN_POINT('Origin',(0.,0.,0.));
#7743=CARTESIAN_POINT('',(-0.335,0.0149999999999999,-4.10256677714363E-17));
#7744=CARTESIAN_POINT('Origin',(0.22,0.,0.));
#7745=CARTESIAN_POINT('',(-0.22,-6.93889390390723E-18,-2.69422295812418E-17));
#7746=CARTESIAN_POINT('Origin',(0.,0.,0.));
#7747=CARTESIAN_POINT('Origin',(0.,-0.02,0.));
#7748=CARTESIAN_POINT('',(-0.1954,-0.0492,2.39295984553393E-17));
#7749=CARTESIAN_POINT('Origin',(0.,-0.0492,0.));
#7750=CARTESIAN_POINT('',(-0.21,-0.02,-2.57175827820944E-17));
#7751=CARTESIAN_POINT('Origin',(0.,-0.8,0.));
#7752=CARTESIAN_POINT('',(-0.1954,-1.5646,2.39295984553393E-17));
#7753=CARTESIAN_POINT('Origin',(0.,-1.5646,0.));
#7754=CARTESIAN_POINT('',(-0.1954,-0.8,-2.39295984553393E-17));
#7755=CARTESIAN_POINT('Origin',(0.,-1.58,0.));
#7756=CARTESIAN_POINT('',(-0.16,-1.6,-1.95943487863577E-17));
#7757=CARTESIAN_POINT('Origin',(0.,-1.6,0.));
#7758=CARTESIAN_POINT('',(-0.18,-1.58,-2.20436423846524E-17));
#7759=CARTESIAN_POINT('Origin',(0.,-1.6,0.));
#7760=CARTESIAN_POINT('Origin',(0.0866025403784439,-0.4,-0.15));
#7761=CARTESIAN_POINT('',(0.173205080756888,-0.4,0.));
#7762=CARTESIAN_POINT('',(0.0866025403784439,-0.4,-0.15));
#7763=CARTESIAN_POINT('',(0.173205080756888,-0.4,0.));
#7764=CARTESIAN_POINT('',(0.0866025403784439,-0.64,-0.15));
#7765=CARTESIAN_POINT('',(0.0866025403784439,-0.4,-0.15));
#7766=CARTESIAN_POINT('',(0.173205080756888,-0.64,0.));
#7767=CARTESIAN_POINT('',(0.173205080756888,-0.64,0.));
#7768=CARTESIAN_POINT('',(0.173205080756888,-0.4,0.));
#7769=CARTESIAN_POINT('Origin',(-0.0866025403784438,-0.4,-0.15));
#7770=CARTESIAN_POINT('',(-0.0866025403784438,-0.4,-0.15));
#7771=CARTESIAN_POINT('',(0.0866025403784439,-0.4,-0.15));
#7772=CARTESIAN_POINT('',(-0.0866025403784438,-0.64,-0.15));
#7773=CARTESIAN_POINT('',(-0.0866025403784438,-0.4,-0.15));
#7774=CARTESIAN_POINT('',(0.0866025403784439,-0.64,-0.15));
#7775=CARTESIAN_POINT('Origin',(-0.173205080756888,-0.4,-2.77555756156289E-17));
#7776=CARTESIAN_POINT('',(-0.173205080756888,-0.4,-2.12115047744981E-17));
#7777=CARTESIAN_POINT('',(-0.0866025403784438,-0.4,-0.15));
#7778=CARTESIAN_POINT('',(-0.173205080756888,-0.64,-2.77555756156289E-17));
#7779=CARTESIAN_POINT('',(-0.173205080756888,-0.4,-2.12115047744981E-17));
#7780=CARTESIAN_POINT('',(-0.0866025403784438,-0.64,-0.15));
#7781=CARTESIAN_POINT('Origin',(-0.0866025403784439,-0.4,0.15));
#7782=CARTESIAN_POINT('',(-0.0866025403784439,-0.4,0.15));
#7783=CARTESIAN_POINT('',(-0.173205080756888,-0.4,-2.12115047744981E-17));
#7784=CARTESIAN_POINT('',(-0.0866025403784439,-0.64,0.15));
#7785=CARTESIAN_POINT('',(-0.0866025403784439,-0.4,0.15));
#7786=CARTESIAN_POINT('',(-0.173205080756888,-0.64,-2.12115047744981E-17));
#7787=CARTESIAN_POINT('Origin',(0.0866025403784439,-0.4,0.15));
#7788=CARTESIAN_POINT('',(0.0866025403784439,-0.4,0.15));
#7789=CARTESIAN_POINT('',(-0.0866025403784439,-0.4,0.15));
#7790=CARTESIAN_POINT('',(0.0866025403784439,-0.64,0.15));
#7791=CARTESIAN_POINT('',(0.0866025403784439,-0.4,0.15));
#7792=CARTESIAN_POINT('',(-0.0866025403784439,-0.64,0.15));
#7793=CARTESIAN_POINT('Origin',(0.173205080756888,-0.4,0.));
#7794=CARTESIAN_POINT('',(0.0866025403784439,-0.4,0.15));
#7795=CARTESIAN_POINT('',(0.0866025403784439,-0.64,0.15));
#7796=CARTESIAN_POINT('Origin',(0.,-0.4,-2.77555756156289E-17));
#7797=CARTESIAN_POINT('Origin',(0.,-0.64,-2.77555756156289E-17));
#8461=UNCERTAINTY_MEASURE_WITH_UNIT(LENGTH_MEASURE(0.001),#8500,
'DISTANCE_ACCURACY_VALUE',
'Maximum model space distance between geometric entities at asserted c
onnectivities');
#8476=UNCERTAINTY_MEASURE_WITH_UNIT(LENGTH_MEASURE(0.001),#8500,
'DISTANCE_ACCURACY_VALUE',
'Maximum model space distance between geometric entities at asserted c
onnectivities');
#8484=(
GEOMETRIC_REPRESENTATION_CONTEXT(3)
GLOBAL_UNCERTAINTY_ASSIGNED_CONTEXT((#8461))
GLOBAL_UNIT_ASSIGNED_CONTEXT((#8500,#8502,#8503))
REPRESENTATION_CONTEXT('','3D')
);
#8499=(
GEOMETRIC_REPRESENTATION_CONTEXT(3)
GLOBAL_UNCERTAINTY_ASSIGNED_CONTEXT((#8476))
GLOBAL_UNIT_ASSIGNED_CONTEXT((#8500,#8502,#8503))
REPRESENTATION_CONTEXT('','3D')
);
#8500=(
LENGTH_UNIT()
NAMED_UNIT(*)
SI_UNIT(.CENTI.,.METRE.)
);
#8502=(
NAMED_UNIT(*)
PLANE_ANGLE_UNIT()
SI_UNIT($,.RADIAN.)
);
#8503=(
NAMED_UNIT(*)
SI_UNIT($,.STERADIAN.)
SOLID_ANGLE_UNIT()
);
#8511=SHAPE_DEFINITION_REPRESENTATION(#8533,#8605);
#8533=PRODUCT_DEFINITION_SHAPE('',$,#8628);
#8605=SHAPE_REPRESENTATION('',(#5351),#8484);
#8620=PRODUCT_DEFINITION_CONTEXT('part definition',#8688,'design');
#8628=PRODUCT_DEFINITION('Cap Screw - M4x16','Cap Screw - M4x16',#8650,
#8620);
#8650=PRODUCT_DEFINITION_FORMATION('',$,#8697);
#8688=APPLICATION_CONTEXT(
'Core Data for Automotive Mechanical Design Process');
#8689=PRODUCT_CONTEXT('part definition',#8688,'mechanical');
#8697=PRODUCT('Cap Screw - M4x16','Cap Screw - M4x16',
'Cap Screw - M4x16',(#8689));
#8789=COLOUR_RGB('Black',0.12,0.14,0.17);
#8790=FILL_AREA_STYLE_COLOUR('',#8789);
#8791=FILL_AREA_STYLE('',(#8790));
#8792=SURFACE_STYLE_FILL_AREA(#8791);
#8793=SURFACE_SIDE_STYLE('',(#8792));
#8794=SURFACE_STYLE_USAGE(.BOTH.,#8793);
#8795=PRESENTATION_STYLE_ASSIGNMENT((#8794));
ENDSEC;
END-ISO-10303-21;
